ISO-10303-21;
HEADER;
/* Generated by software containing ST-Developer
 * from STEP Tools, Inc. (www.steptools.com) 
 */

FILE_DESCRIPTION(
/* description */ ('Two-link friction support arm'),
/* implementation_level */ '2;1');

FILE_NAME(
/* name */ 'Captive slot nut.step',
/* time_stamp */ '2026-10-27T20:01:49-07:00',
/* author */ (''),
/* organization */ (''),
/* preprocessor_version */ 'ST-DEVELOPER v20.2',
/* originating_system */ 'Autodesk Translation Framework v15.17.0.0',
/* authorisation */ '');

FILE_SCHEMA (('AUTOMOTIVE_DESIGN { 1 0 10303 214 3 1 1 }'));
ENDSEC;

DATA;
#10=MECHANICAL_DESIGN_GEOMETRIC_PRESENTATION_REPRESENTATION('',(#197),#5492);
#171=ELLIPSE('',#3388,0.299389011154384,0.2117);
#172=ELLIPSE('',#3392,0.299389011154384,0.2117);
#175=SHAPE_REPRESENTATION_RELATIONSHIP('SRR','None',#5566,#186);
#186=ADVANCED_BREP_SHAPE_REPRESENTATION('',(#208),#5480);
#197=STYLED_ITEM('',(#5708),#208);
#208=MANIFOLD_SOLID_BREP('Body1',#3173);
#224=FACE_BOUND('',#611,.T.);
#306=PLANE('',#3378);
#307=PLANE('',#3379);
#308=PLANE('',#3380);
#309=PLANE('',#3382);
#310=PLANE('',#3383);
#311=PLANE('',#3384);
#312=PLANE('',#3385);
#313=PLANE('',#3386);
#314=PLANE('',#3387);
#315=PLANE('',#3394);
#316=PLANE('',#3395);
#317=PLANE('',#3396);
#318=PLANE('',#3397);
#433=FACE_OUTER_BOUND('',#608,.T.);
#434=FACE_OUTER_BOUND('',#609,.T.);
#435=FACE_OUTER_BOUND('',#610,.T.);
#436=FACE_OUTER_BOUND('',#612,.T.);
#437=FACE_OUTER_BOUND('',#613,.T.);
#438=FACE_OUTER_BOUND('',#614,.T.);
#439=FACE_OUTER_BOUND('',#615,.T.);
#440=FACE_OUTER_BOUND('',#616,.T.);
#441=FACE_OUTER_BOUND('',#617,.T.);
#442=FACE_OUTER_BOUND('',#618,.T.);
#443=FACE_OUTER_BOUND('',#619,.T.);
#444=FACE_OUTER_BOUND('',#620,.T.);
#445=FACE_OUTER_BOUND('',#621,.T.);
#446=FACE_OUTER_BOUND('',#622,.T.);
#608=EDGE_LOOP('',(#2474,#2475,#2476,#2477));
#609=EDGE_LOOP('',(#2478,#2479,#2480,#2481));
#610=EDGE_LOOP('',(#2482,#2483,#2484,#2485));
#611=EDGE_LOOP('',(#2486));
#612=EDGE_LOOP('',(#2487,#2488,#2489,#2490,#2491,#2492,#2493,#2494,#2495,
#2496));
#613=EDGE_LOOP('',(#2497,#2498,#2499,#2500));
#614=EDGE_LOOP('',(#2501,#2502,#2503,#2504));
#615=EDGE_LOOP('',(#2505,#2506,#2507,#2508,#2509,#2510,#2511,#2512,#2513,
#2514));
#616=EDGE_LOOP('',(#2515,#2516,#2517,#2518));
#617=EDGE_LOOP('',(#2519,#2520,#2521,#2522,#2523,#2524));
#618=EDGE_LOOP('',(#2525,#2526,#2527,#2528,#2529,#2530,#2531,#2532));
#619=EDGE_LOOP('',(#2533,#2534,#2535,#2536,#2537));
#620=EDGE_LOOP('',(#2538,#2539,#2540,#2541));
#621=EDGE_LOOP('',(#2542,#2543,#2544,#2545,#2546,#2547));
#622=EDGE_LOOP('',(#2548,#2549,#2550,#2551));
#901=LINE('',#4866,#1214);
#902=LINE('',#4868,#1215);
#903=LINE('',#4870,#1216);
#904=LINE('',#4871,#1217);
#905=LINE('',#4874,#1218);
#906=LINE('',#4876,#1219);
#907=LINE('',#4877,#1220);
#908=LINE('',#4880,#1221);
#909=LINE('',#4882,#1222);
#910=LINE('',#4883,#1223);
#911=LINE('',#4888,#1224);
#912=LINE('',#4890,#1225);
#913=LINE('',#4892,#1226);
#914=LINE('',#4894,#1227);
#915=LINE('',#4896,#1228);
#916=LINE('',#4898,#1229);
#917=LINE('',#4899,#1230);
#918=LINE('',#4902,#1231);
#919=LINE('',#4903,#1232);
#920=LINE('',#4906,#1233);
#921=LINE('',#4907,#1234);
#922=LINE('',#4910,#1235);
#923=LINE('',#4912,#1236);
#924=LINE('',#4914,#1237);
#925=LINE('',#4916,#1238);
#926=LINE('',#4917,#1239);
#927=LINE('',#4919,#1240);
#928=LINE('',#4922,#1241);
#929=LINE('',#4925,#1242);
#930=LINE('',#4929,#1243);
#931=LINE('',#4936,#1244);
#932=LINE('',#4938,#1245);
#933=LINE('',#4940,#1246);
#1214=VECTOR('',#3913,1.);
#1215=VECTOR('',#3914,1.);
#1216=VECTOR('',#3915,1.);
#1217=VECTOR('',#3916,1.);
#1218=VECTOR('',#3919,1.);
#1219=VECTOR('',#3920,1.);
#1220=VECTOR('',#3921,1.);
#1221=VECTOR('',#3924,1.);
#1222=VECTOR('',#3925,1.);
#1223=VECTOR('',#3926,1.);
#1224=VECTOR('',#3931,1.);
#1225=VECTOR('',#3932,1.);
#1226=VECTOR('',#3933,1.);
#1227=VECTOR('',#3934,1.);
#1228=VECTOR('',#3935,1.);
#1229=VECTOR('',#3936,1.);
#1230=VECTOR('',#3937,1.);
#1231=VECTOR('',#3940,1.);
#1232=VECTOR('',#3941,1.);
#1233=VECTOR('',#3944,1.);
#1234=VECTOR('',#3945,1.);
#1235=VECTOR('',#3948,1.);
#1236=VECTOR('',#3949,1.);
#1237=VECTOR('',#3950,1.);
#1238=VECTOR('',#3951,1.);
#1239=VECTOR('',#3952,1.);
#1240=VECTOR('',#3955,1.);
#1241=VECTOR('',#3958,1.);
#1242=VECTOR('',#3961,1.);
#1243=VECTOR('',#3966,0.21);
#1244=VECTOR('',#3975,1.);
#1245=VECTOR('',#3978,1.);
#1246=VECTOR('',#3981,1.);
#1375=CIRCLE('',#3381,0.2117);
#1376=CIRCLE('',#3390,0.2117);
#1377=CIRCLE('',#3391,0.2117);
#1378=CIRCLE('',#3393,0.2117);
#1561=VERTEX_POINT('',#4864);
#1562=VERTEX_POINT('',#4865);
#1563=VERTEX_POINT('',#4867);
#1564=VERTEX_POINT('',#4869);
#1565=VERTEX_POINT('',#4873);
#1566=VERTEX_POINT('',#4875);
#1567=VERTEX_POINT('',#4879);
#1568=VERTEX_POINT('',#4881);
#1569=VERTEX_POINT('',#4884);
#1570=VERTEX_POINT('',#4887);
#1571=VERTEX_POINT('',#4889);
#1572=VERTEX_POINT('',#4891);
#1573=VERTEX_POINT('',#4893);
#1574=VERTEX_POINT('',#4895);
#1575=VERTEX_POINT('',#4897);
#1576=VERTEX_POINT('',#4901);
#1577=VERTEX_POINT('',#4905);
#1578=VERTEX_POINT('',#4909);
#1579=VERTEX_POINT('',#4911);
#1580=VERTEX_POINT('',#4913);
#1581=VERTEX_POINT('',#4915);
#1582=VERTEX_POINT('',#4921);
#1583=VERTEX_POINT('',#4923);
#1584=VERTEX_POINT('',#4927);
#1585=VERTEX_POINT('',#4930);
#1586=VERTEX_POINT('',#4932);
#1891=EDGE_CURVE('',#1561,#1562,#901,.T.);
#1892=EDGE_CURVE('',#1563,#1561,#902,.T.);
#1893=EDGE_CURVE('',#1564,#1563,#903,.T.);
#1894=EDGE_CURVE('',#1562,#1564,#904,.T.);
#1895=EDGE_CURVE('',#1563,#1565,#905,.T.);
#1896=EDGE_CURVE('',#1566,#1565,#906,.T.);
#1897=EDGE_CURVE('',#1564,#1566,#907,.T.);
#1898=EDGE_CURVE('',#1565,#1567,#908,.T.);
#1899=EDGE_CURVE('',#1567,#1568,#909,.T.);
#1900=EDGE_CURVE('',#1568,#1566,#910,.T.);
#1901=EDGE_CURVE('',#1569,#1569,#1375,.T.);
#1902=EDGE_CURVE('',#1570,#1561,#911,.T.);
#1903=EDGE_CURVE('',#1571,#1570,#912,.T.);
#1904=EDGE_CURVE('',#1571,#1572,#913,.T.);
#1905=EDGE_CURVE('',#1573,#1572,#914,.T.);
#1906=EDGE_CURVE('',#1573,#1574,#915,.T.);
#1907=EDGE_CURVE('',#1574,#1575,#916,.T.);
#1908=EDGE_CURVE('',#1575,#1567,#917,.T.);
#1909=EDGE_CURVE('',#1575,#1576,#918,.T.);
#1910=EDGE_CURVE('',#1576,#1568,#919,.T.);
#1911=EDGE_CURVE('',#1577,#1574,#920,.T.);
#1912=EDGE_CURVE('',#1576,#1577,#921,.T.);
#1913=EDGE_CURVE('',#1578,#1577,#922,.T.);
#1914=EDGE_CURVE('',#1579,#1578,#923,.T.);
#1915=EDGE_CURVE('',#1579,#1580,#924,.T.);
#1916=EDGE_CURVE('',#1581,#1580,#925,.T.);
#1917=EDGE_CURVE('',#1581,#1562,#926,.T.);
#1918=EDGE_CURVE('',#1578,#1573,#927,.T.);
#1919=EDGE_CURVE('',#1572,#1582,#928,.T.);
#1920=EDGE_CURVE('',#1582,#1583,#171,.T.);
#1921=EDGE_CURVE('',#1583,#1579,#929,.T.);
#1922=EDGE_CURVE('',#1584,#1582,#1376,.F.);
#1923=EDGE_CURVE('',#1584,#1569,#930,.T.);
#1924=EDGE_CURVE('',#1585,#1584,#1377,.F.);
#1925=EDGE_CURVE('',#1586,#1585,#172,.T.);
#1926=EDGE_CURVE('',#1583,#1586,#1378,.F.);
#1927=EDGE_CURVE('',#1585,#1571,#931,.T.);
#1928=EDGE_CURVE('',#1580,#1586,#932,.T.);
#1929=EDGE_CURVE('',#1570,#1581,#933,.T.);
#2474=ORIENTED_EDGE('',*,*,#1891,.F.);
#2475=ORIENTED_EDGE('',*,*,#1892,.F.);
#2476=ORIENTED_EDGE('',*,*,#1893,.F.);
#2477=ORIENTED_EDGE('',*,*,#1894,.F.);
#2478=ORIENTED_EDGE('',*,*,#1893,.T.);
#2479=ORIENTED_EDGE('',*,*,#1895,.T.);
#2480=ORIENTED_EDGE('',*,*,#1896,.F.);
#2481=ORIENTED_EDGE('',*,*,#1897,.F.);
#2482=ORIENTED_EDGE('',*,*,#1898,.T.);
#2483=ORIENTED_EDGE('',*,*,#1899,.T.);
#2484=ORIENTED_EDGE('',*,*,#1900,.T.);
#2485=ORIENTED_EDGE('',*,*,#1896,.T.);
#2486=ORIENTED_EDGE('',*,*,#1901,.T.);
#2487=ORIENTED_EDGE('',*,*,#1898,.F.);
#2488=ORIENTED_EDGE('',*,*,#1895,.F.);
#2489=ORIENTED_EDGE('',*,*,#1892,.T.);
#2490=ORIENTED_EDGE('',*,*,#1902,.F.);
#2491=ORIENTED_EDGE('',*,*,#1903,.F.);
#2492=ORIENTED_EDGE('',*,*,#1904,.T.);
#2493=ORIENTED_EDGE('',*,*,#1905,.F.);
#2494=ORIENTED_EDGE('',*,*,#1906,.T.);
#2495=ORIENTED_EDGE('',*,*,#1907,.T.);
#2496=ORIENTED_EDGE('',*,*,#1908,.T.);
#2497=ORIENTED_EDGE('',*,*,#1909,.T.);
#2498=ORIENTED_EDGE('',*,*,#1910,.T.);
#2499=ORIENTED_EDGE('',*,*,#1899,.F.);
#2500=ORIENTED_EDGE('',*,*,#1908,.F.);
#2501=ORIENTED_EDGE('',*,*,#1911,.F.);
#2502=ORIENTED_EDGE('',*,*,#1912,.F.);
#2503=ORIENTED_EDGE('',*,*,#1909,.F.);
#2504=ORIENTED_EDGE('',*,*,#1907,.F.);
#2505=ORIENTED_EDGE('',*,*,#1900,.F.);
#2506=ORIENTED_EDGE('',*,*,#1910,.F.);
#2507=ORIENTED_EDGE('',*,*,#1912,.T.);
#2508=ORIENTED_EDGE('',*,*,#1913,.F.);
#2509=ORIENTED_EDGE('',*,*,#1914,.F.);
#2510=ORIENTED_EDGE('',*,*,#1915,.T.);
#2511=ORIENTED_EDGE('',*,*,#1916,.F.);
#2512=ORIENTED_EDGE('',*,*,#1917,.T.);
#2513=ORIENTED_EDGE('',*,*,#1894,.T.);
#2514=ORIENTED_EDGE('',*,*,#1897,.T.);
#2515=ORIENTED_EDGE('',*,*,#1911,.T.);
#2516=ORIENTED_EDGE('',*,*,#1906,.F.);
#2517=ORIENTED_EDGE('',*,*,#1918,.F.);
#2518=ORIENTED_EDGE('',*,*,#1913,.T.);
#2519=ORIENTED_EDGE('',*,*,#1914,.T.);
#2520=ORIENTED_EDGE('',*,*,#1918,.T.);
#2521=ORIENTED_EDGE('',*,*,#1905,.T.);
#2522=ORIENTED_EDGE('',*,*,#1919,.T.);
#2523=ORIENTED_EDGE('',*,*,#1920,.T.);
#2524=ORIENTED_EDGE('',*,*,#1921,.T.);
#2525=ORIENTED_EDGE('',*,*,#1920,.F.);
#2526=ORIENTED_EDGE('',*,*,#1922,.F.);
#2527=ORIENTED_EDGE('',*,*,#1923,.T.);
#2528=ORIENTED_EDGE('',*,*,#1901,.F.);
#2529=ORIENTED_EDGE('',*,*,#1923,.F.);
#2530=ORIENTED_EDGE('',*,*,#1924,.F.);
#2531=ORIENTED_EDGE('',*,*,#1925,.F.);
#2532=ORIENTED_EDGE('',*,*,#1926,.F.);
#2533=ORIENTED_EDGE('',*,*,#1919,.F.);
#2534=ORIENTED_EDGE('',*,*,#1904,.F.);
#2535=ORIENTED_EDGE('',*,*,#1927,.F.);
#2536=ORIENTED_EDGE('',*,*,#1924,.T.);
#2537=ORIENTED_EDGE('',*,*,#1922,.T.);
#2538=ORIENTED_EDGE('',*,*,#1921,.F.);
#2539=ORIENTED_EDGE('',*,*,#1926,.T.);
#2540=ORIENTED_EDGE('',*,*,#1928,.F.);
#2541=ORIENTED_EDGE('',*,*,#1915,.F.);
#2542=ORIENTED_EDGE('',*,*,#1903,.T.);
#2543=ORIENTED_EDGE('',*,*,#1929,.T.);
#2544=ORIENTED_EDGE('',*,*,#1916,.T.);
#2545=ORIENTED_EDGE('',*,*,#1928,.T.);
#2546=ORIENTED_EDGE('',*,*,#1925,.T.);
#2547=ORIENTED_EDGE('',*,*,#1927,.T.);
#2548=ORIENTED_EDGE('',*,*,#1891,.T.);
#2549=ORIENTED_EDGE('',*,*,#1917,.F.);
#2550=ORIENTED_EDGE('',*,*,#1929,.F.);
#2551=ORIENTED_EDGE('',*,*,#1902,.T.);
#2972=CYLINDRICAL_SURFACE('',#3389,0.2117);
#3064=ADVANCED_FACE('',(#433),#306,.F.);
#3065=ADVANCED_FACE('',(#434),#307,.T.);
#3066=ADVANCED_FACE('',(#435,#224),#308,.T.);
#3067=ADVANCED_FACE('',(#436),#309,.T.);
#3068=ADVANCED_FACE('',(#437),#310,.T.);
#3069=ADVANCED_FACE('',(#438),#311,.F.);
#3070=ADVANCED_FACE('',(#439),#312,.T.);
#3071=ADVANCED_FACE('',(#440),#313,.T.);
#3072=ADVANCED_FACE('',(#441),#314,.T.);
#3073=ADVANCED_FACE('',(#442),#2972,.F.);
#3074=ADVANCED_FACE('',(#443),#315,.F.);
#3075=ADVANCED_FACE('',(#444),#316,.F.);
#3076=ADVANCED_FACE('',(#445),#317,.T.);
#3077=ADVANCED_FACE('',(#446),#318,.T.);
#3173=CLOSED_SHELL('',(#3064,#3065,#3066,#3067,#3068,#3069,#3070,#3071,
#3072,#3073,#3074,#3075,#3076,#3077));
#3377=AXIS2_PLACEMENT_3D('',#4862,#3909,#3910);
#3378=AXIS2_PLACEMENT_3D('',#4863,#3911,#3912);
#3379=AXIS2_PLACEMENT_3D('',#4872,#3917,#3918);
#3380=AXIS2_PLACEMENT_3D('',#4878,#3922,#3923);
#3381=AXIS2_PLACEMENT_3D('',#4885,#3927,#3928);
#3382=AXIS2_PLACEMENT_3D('',#4886,#3929,#3930);
#3383=AXIS2_PLACEMENT_3D('',#4900,#3938,#3939);
#3384=AXIS2_PLACEMENT_3D('',#4904,#3942,#3943);
#3385=AXIS2_PLACEMENT_3D('',#4908,#3946,#3947);
#3386=AXIS2_PLACEMENT_3D('',#4918,#3953,#3954);
#3387=AXIS2_PLACEMENT_3D('',#4920,#3956,#3957);
#3388=AXIS2_PLACEMENT_3D('',#4924,#3959,#3960);
#3389=AXIS2_PLACEMENT_3D('',#4926,#3962,#3963);
#3390=AXIS2_PLACEMENT_3D('',#4928,#3964,#3965);
#3391=AXIS2_PLACEMENT_3D('',#4931,#3967,#3968);
#3392=AXIS2_PLACEMENT_3D('',#4933,#3969,#3970);
#3393=AXIS2_PLACEMENT_3D('',#4934,#3971,#3972);
#3394=AXIS2_PLACEMENT_3D('',#4935,#3973,#3974);
#3395=AXIS2_PLACEMENT_3D('',#4937,#3976,#3977);
#3396=AXIS2_PLACEMENT_3D('',#4939,#3979,#3980);
#3397=AXIS2_PLACEMENT_3D('',#4941,#3982,#3983);
#3909=DIRECTION('axis',(0.,0.,1.));
#3910=DIRECTION('refdir',(1.,0.,0.));
#3911=DIRECTION('center_axis',(0.,0.,1.));
#3912=DIRECTION('ref_axis',(1.,0.,0.));
#3913=DIRECTION('',(1.,0.,0.));
#3914=DIRECTION('',(0.,-1.,0.));
#3915=DIRECTION('',(-1.,0.,0.));
#3916=DIRECTION('',(0.,1.,0.));
#3917=DIRECTION('center_axis',(0.,1.,0.));
#3918=DIRECTION('ref_axis',(-1.,0.,0.));
#3919=DIRECTION('',(0.,0.,1.));
#3920=DIRECTION('',(-1.,0.,0.));
#3921=DIRECTION('',(0.,0.,1.));
#3922=DIRECTION('center_axis',(0.,0.,1.));
#3923=DIRECTION('ref_axis',(1.,0.,0.));
#3924=DIRECTION('',(0.,-1.,0.));
#3925=DIRECTION('',(1.,0.,0.));
#3926=DIRECTION('',(0.,1.,0.));
#3927=DIRECTION('center_axis',(0.,0.,-1.));
#3928=DIRECTION('ref_axis',(1.,0.,0.));
#3929=DIRECTION('center_axis',(-1.,0.,0.));
#3930=DIRECTION('ref_axis',(0.,-1.,0.));
#3931=DIRECTION('',(0.,0.,1.));
#3932=DIRECTION('',(0.,0.707106781186548,0.707106781186548));
#3933=DIRECTION('',(0.,-1.,0.));
#3934=DIRECTION('',(0.,0.707106781186548,-0.707106781186548));
#3935=DIRECTION('',(0.,0.,1.));
#3936=DIRECTION('',(0.,-1.,0.));
#3937=DIRECTION('',(0.,0.,1.));
#3938=DIRECTION('center_axis',(0.,-1.,0.));
#3939=DIRECTION('ref_axis',(1.,0.,0.));
#3940=DIRECTION('',(1.,0.,0.));
#3941=DIRECTION('',(0.,0.,1.));
#3942=DIRECTION('center_axis',(0.,0.,1.));
#3943=DIRECTION('ref_axis',(1.,0.,0.));
#3944=DIRECTION('',(-1.,0.,0.));
#3945=DIRECTION('',(0.,1.,0.));
#3946=DIRECTION('center_axis',(1.,0.,0.));
#3947=DIRECTION('ref_axis',(0.,1.,0.));
#3948=DIRECTION('',(0.,0.,1.));
#3949=DIRECTION('',(0.,-0.707106781186548,0.707106781186548));
#3950=DIRECTION('',(0.,1.,0.));
#3951=DIRECTION('',(0.,-0.707106781186548,-0.707106781186548));
#3952=DIRECTION('',(0.,0.,1.));
#3953=DIRECTION('center_axis',(0.,-1.,0.));
#3954=DIRECTION('ref_axis',(1.,0.,0.));
#3955=DIRECTION('',(-1.,0.,0.));
#3956=DIRECTION('center_axis',(0.,-0.707106781186548,-0.707106781186548));
#3957=DIRECTION('ref_axis',(-1.,0.,0.));
#3958=DIRECTION('',(1.,0.,0.));
#3959=DIRECTION('center_axis',(0.,0.707106781186548,0.707106781186548));
#3960=DIRECTION('ref_axis',(0.,0.707106781186547,-0.707106781186547));
#3961=DIRECTION('',(1.,0.,0.));
#3962=DIRECTION('center_axis',(0.,0.,1.));
#3963=DIRECTION('ref_axis',(1.,0.,0.));
#3964=DIRECTION('center_axis',(0.,0.,-1.));
#3965=DIRECTION('ref_axis',(1.,0.,0.));
#3966=DIRECTION('',(0.,0.,1.));
#3967=DIRECTION('center_axis',(0.,0.,-1.));
#3968=DIRECTION('ref_axis',(1.,0.,0.));
#3969=DIRECTION('center_axis',(0.,-0.707106781186548,0.707106781186548));
#3970=DIRECTION('ref_axis',(0.,0.707106781186547,0.707106781186547));
#3971=DIRECTION('center_axis',(0.,0.,-1.));
#3972=DIRECTION('ref_axis',(1.,0.,0.));
#3973=DIRECTION('center_axis',(0.,0.,1.));
#3974=DIRECTION('ref_axis',(1.,0.,0.));
#3975=DIRECTION('',(-1.,0.,0.));
#3976=DIRECTION('center_axis',(0.,0.,1.));
#3977=DIRECTION('ref_axis',(1.,0.,0.));
#3978=DIRECTION('',(-1.,0.,0.));
#3979=DIRECTION('center_axis',(0.,0.707106781186548,-0.707106781186548));
#3980=DIRECTION('ref_axis',(-1.,0.,0.));
#3981=DIRECTION('',(1.,0.,0.));
#3982=DIRECTION('center_axis',(0.,1.,0.));
#3983=DIRECTION('ref_axis',(-1.,0.,0.));
#4862=CARTESIAN_POINT('',(0.,0.,0.));
#4863=CARTESIAN_POINT('Origin',(0.,0.395,0.25));
#4864=CARTESIAN_POINT('',(-0.5,0.3,0.25));
#4865=CARTESIAN_POINT('',(0.5,0.3,0.25));
#4866=CARTESIAN_POINT('',(0.25,0.3,0.25));
#4867=CARTESIAN_POINT('',(-0.5,0.5,0.25));
#4868=CARTESIAN_POINT('',(-0.5,0.5,0.25));
#4869=CARTESIAN_POINT('',(0.5,0.5,0.25));
#4870=CARTESIAN_POINT('',(0.5,0.5,0.25));
#4871=CARTESIAN_POINT('',(0.5,0.29,0.25));
#4872=CARTESIAN_POINT('Origin',(0.5,0.5,0.25));
#4873=CARTESIAN_POINT('',(-0.5,0.5,0.4));
#4874=CARTESIAN_POINT('',(-0.5,0.5,0.25));
#4875=CARTESIAN_POINT('',(0.5,0.5,0.4));
#4876=CARTESIAN_POINT('',(0.5,0.5,0.4));
#4877=CARTESIAN_POINT('',(0.5,0.5,0.25));
#4878=CARTESIAN_POINT('Origin',(0.,0.,0.4));
#4879=CARTESIAN_POINT('',(-0.5,-0.5,0.4));
#4880=CARTESIAN_POINT('',(-0.5,0.5,0.4));
#4881=CARTESIAN_POINT('',(0.5,-0.5,0.4));
#4882=CARTESIAN_POINT('',(-0.5,-0.5,0.4));
#4883=CARTESIAN_POINT('',(0.5,-0.3,0.4));
#4884=CARTESIAN_POINT('',(-0.2117,2.59257727379495E-17,0.4));
#4885=CARTESIAN_POINT('Origin',(0.,0.,0.4));
#4886=CARTESIAN_POINT('Origin',(-0.5,0.3,0.));
#4887=CARTESIAN_POINT('',(-0.5,0.3,0.15));
#4888=CARTESIAN_POINT('',(-0.5,0.3,0.));
#4889=CARTESIAN_POINT('',(-0.5,0.15,0.));
#4890=CARTESIAN_POINT('',(-0.5,0.225,0.075));
#4891=CARTESIAN_POINT('',(-0.5,-0.15,0.));
#4892=CARTESIAN_POINT('',(-0.5,0.3,0.));
#4893=CARTESIAN_POINT('',(-0.5,-0.3,0.15));
#4894=CARTESIAN_POINT('',(-0.5,-0.075,-0.075));
#4895=CARTESIAN_POINT('',(-0.5,-0.3,0.25));
#4896=CARTESIAN_POINT('',(-0.5,-0.3,0.));
#4897=CARTESIAN_POINT('',(-0.5,-0.5,0.25));
#4898=CARTESIAN_POINT('',(-0.5,-0.29,0.25));
#4899=CARTESIAN_POINT('',(-0.5,-0.5,0.25));
#4900=CARTESIAN_POINT('Origin',(-0.5,-0.5,0.25));
#4901=CARTESIAN_POINT('',(0.5,-0.5,0.25));
#4902=CARTESIAN_POINT('',(-0.5,-0.5,0.25));
#4903=CARTESIAN_POINT('',(0.5,-0.5,0.25));
#4904=CARTESIAN_POINT('Origin',(0.,-0.395,0.25));
#4905=CARTESIAN_POINT('',(0.5,-0.3,0.25));
#4906=CARTESIAN_POINT('',(-0.25,-0.3,0.25));
#4907=CARTESIAN_POINT('',(0.5,-0.5,0.25));
#4908=CARTESIAN_POINT('Origin',(0.5,-0.3,0.));
#4909=CARTESIAN_POINT('',(0.5,-0.3,0.15));
#4910=CARTESIAN_POINT('',(0.5,-0.3,0.));
#4911=CARTESIAN_POINT('',(0.5,-0.15,0.));
#4912=CARTESIAN_POINT('',(0.5,-0.225,0.075));
#4913=CARTESIAN_POINT('',(0.5,0.15,0.));
#4914=CARTESIAN_POINT('',(0.5,-0.3,0.));
#4915=CARTESIAN_POINT('',(0.5,0.3,0.15));
#4916=CARTESIAN_POINT('',(0.5,0.075,-0.075));
#4917=CARTESIAN_POINT('',(0.5,0.3,0.));
#4918=CARTESIAN_POINT('Origin',(-0.5,-0.3,0.));
#4919=CARTESIAN_POINT('',(-0.25,-0.3,0.15));
#4920=CARTESIAN_POINT('Origin',(-0.25,-0.225,0.075));
#4921=CARTESIAN_POINT('',(-0.149388386429468,-0.15,0.));
#4922=CARTESIAN_POINT('',(-0.25,-0.15,0.));
#4923=CARTESIAN_POINT('',(0.149388386429468,-0.15,0.));
#4924=CARTESIAN_POINT('Origin',(0.,0.,-0.15));
#4925=CARTESIAN_POINT('',(-0.25,-0.15,0.));
#4926=CARTESIAN_POINT('Origin',(0.,0.,-0.1));
#4927=CARTESIAN_POINT('',(-0.2117,-2.59257727379495E-17,0.));
#4928=CARTESIAN_POINT('Origin',(0.,0.,0.));
#4929=CARTESIAN_POINT('',(-0.2117,-2.59257727379495E-17,-0.1));
#4930=CARTESIAN_POINT('',(-0.149388386429468,0.15,0.));
#4931=CARTESIAN_POINT('Origin',(0.,0.,0.));
#4932=CARTESIAN_POINT('',(0.149388386429468,0.15,0.));
#4933=CARTESIAN_POINT('Origin',(0.,0.,-0.15));
#4934=CARTESIAN_POINT('Origin',(0.,0.,0.));
#4935=CARTESIAN_POINT('Origin',(0.,0.,0.));
#4936=CARTESIAN_POINT('',(0.25,0.15,0.));
#4937=CARTESIAN_POINT('Origin',(0.,0.,0.));
#4938=CARTESIAN_POINT('',(0.25,0.15,0.));
#4939=CARTESIAN_POINT('Origin',(0.25,0.225,0.075));
#4940=CARTESIAN_POINT('',(0.25,0.3,0.15));
#4941=CARTESIAN_POINT('Origin',(0.5,0.3,0.));
#5463=UNCERTAINTY_MEASURE_WITH_UNIT(LENGTH_MEASURE(0.001),#5493,
'DISTANCE_ACCURACY_VALUE',
'Maximum model space distance between geometric entities at asserted c
onnectivities');
#5475=UNCERTAINTY_MEASURE_WITH_UNIT(LENGTH_MEASURE(0.001),#5493,
'DISTANCE_ACCURACY_VALUE',
'Maximum model space distance between geometric entities at asserted c
onnectivities');
#5480=(
GEOMETRIC_REPRESENTATION_CONTEXT(3)
GLOBAL_UNCERTAINTY_ASSIGNED_CONTEXT((#5463))
GLOBAL_UNIT_ASSIGNED_CONTEXT((#5493,#5495,#5496))
REPRESENTATION_CONTEXT('','3D')
);
#5492=(
GEOMETRIC_REPRESENTATION_CONTEXT(3)
GLOBAL_UNCERTAINTY_ASSIGNED_CONTEXT((#5475))
GLOBAL_UNIT_ASSIGNED_CONTEXT((#5493,#5495,#5496))
REPRESENTATION_CONTEXT('','3D')
);
#5493=(
LENGTH_UNIT()
NAMED_UNIT(*)
SI_UNIT(.CENTI.,.METRE.)
);
#5495=(
NAMED_UNIT(*)
PLANE_ANGLE_UNIT()
SI_UNIT($,.RADIAN.)
);
#5496=(
NAMED_UNIT(*)
SI_UNIT($,.STERADIAN.)
SOLID_ANGLE_UNIT()
);
#5501=SHAPE_DEFINITION_REPRESENTATION(#5517,#5566);
#5517=PRODUCT_DEFINITION_SHAPE('',$,#5583);
#5566=SHAPE_REPRESENTATION('',(#3377),#5480);
#5578=PRODUCT_DEFINITION_CONTEXT('part definition',#5628,'design');
#5583=PRODUCT_DEFINITION('Captive slot nut','Captive slot nut',#5599,#5578);
#5599=PRODUCT_DEFINITION_FORMATION('',$,#5634);
#5628=APPLICATION_CONTEXT(
'Core Data for Automotive Mechanical Design Process');
#5629=PRODUCT_CONTEXT('part definition',#5628,'mechanical');
#5634=PRODUCT('Captive slot nut','Captive slot nut','Captive slot nut',
(#5629));
#5702=COLOUR_RGB('Black',0.12,0.14,0.17);
#5703=FILL_AREA_STYLE_COLOUR('',#5702);
#5704=FILL_AREA_STYLE('',(#5703));
#5705=SURFACE_STYLE_FILL_AREA(#5704);
#5706=SURFACE_SIDE_STYLE('',(#5705));
#5707=SURFACE_STYLE_USAGE(.BOTH.,#5706);
#5708=PRESENTATION_STYLE_ASSIGNMENT((#5707));
ENDSEC;
END-ISO-10303-21;
